ISO-10303-21;
HEADER;
/* Generated by software containing ST-Developer
 * from STEP Tools, Inc. (www.steptools.com) 
 */

FILE_DESCRIPTION(
/* description */ ('Fork-mounted skate wheel'),
/* implementation_level */ '2;1');

FILE_NAME(
/* name */ 'M4x10 Cap Screw.step',
/* time_stamp */ '2026-10-29T16:11:26-07:00',
/* author */ (''),
/* organization */ (''),
/* preprocessor_version */ 'ST-DEVELOPER v20.2',
/* originating_system */ 'Autodesk Translation Framework v15.17.0.0',
/* authorisation */ '');

FILE_SCHEMA (('AUTOMOTIVE_DESIGN { 1 0 10303 214 3 1 1 }'));
ENDSEC;

DATA;
#10=MECHANICAL_DESIGN_GEOMETRIC_PRESENTATION_REPRESENTATION('',(#150),#3688);
#113=CONICAL_SURFACE('',#2042,0.325,0.785398163397448);
#114=CONICAL_SURFACE('',#2046,0.335,0.785398163397448);
#115=CONICAL_SURFACE('',#2050,0.21,0.463647609000806);
#120=ORIENTED_CLOSED_SHELL('',*,#1811,.F.);
#121=BREP_WITH_VOIDS('Body1',#1812,(#120));
#126=SHAPE_REPRESENTATION_RELATIONSHIP('SRR','None',#3749,#138);
#138=ADVANCED_BREP_SHAPE_REPRESENTATION('',(#121),#3678);
#150=STYLED_ITEM('',(#3903),#121);
#203=FACE_BOUND('',#460,.T.);
#243=PLANE('',#2030);
#244=PLANE('',#2031);
#245=PLANE('',#2032);
#246=PLANE('',#2033);
#247=PLANE('',#2034);
#248=PLANE('',#2035);
#249=PLANE('',#2036);
#250=PLANE('',#2037);
#251=PLANE('',#2038);
#252=PLANE('',#2040);
#253=PLANE('',#2048);
#313=FACE_OUTER_BOUND('',#446,.T.);
#314=FACE_OUTER_BOUND('',#447,.T.);
#315=FACE_OUTER_BOUND('',#448,.T.);
#316=FACE_OUTER_BOUND('',#449,.T.);
#317=FACE_OUTER_BOUND('',#450,.T.);
#318=FACE_OUTER_BOUND('',#451,.T.);
#319=FACE_OUTER_BOUND('',#452,.T.);
#320=FACE_OUTER_BOUND('',#453,.T.);
#321=FACE_OUTER_BOUND('',#454,.T.);
#322=FACE_OUTER_BOUND('',#455,.T.);
#323=FACE_OUTER_BOUND('',#456,.T.);
#324=FACE_OUTER_BOUND('',#457,.T.);
#325=FACE_OUTER_BOUND('',#458,.T.);
#326=FACE_OUTER_BOUND('',#459,.T.);
#327=FACE_OUTER_BOUND('',#461,.T.);
#328=FACE_OUTER_BOUND('',#462,.T.);
#446=EDGE_LOOP('',(#1367,#1368,#1369,#1370));
#447=EDGE_LOOP('',(#1371,#1372,#1373,#1374));
#448=EDGE_LOOP('',(#1375,#1376,#1377,#1378));
#449=EDGE_LOOP('',(#1379,#1380,#1381,#1382));
#450=EDGE_LOOP('',(#1383,#1384,#1385,#1386));
#451=EDGE_LOOP('',(#1387,#1388,#1389,#1390));
#452=EDGE_LOOP('',(#1391,#1392,#1393,#1394,#1395,#1396));
#453=EDGE_LOOP('',(#1397,#1398,#1399,#1400,#1401,#1402));
#454=EDGE_LOOP('',(#1403));
#455=EDGE_LOOP('',(#1404));
#456=EDGE_LOOP('',(#1405,#1406,#1407,#1408));
#457=EDGE_LOOP('',(#1409,#1410,#1411,#1412));
#458=EDGE_LOOP('',(#1413,#1414,#1415,#1416));
#459=EDGE_LOOP('',(#1417));
#460=EDGE_LOOP('',(#1418));
#461=EDGE_LOOP('',(#1419,#1420,#1421,#1422));
#462=EDGE_LOOP('',(#1423,#1424,#1425,#1426));
#587=LINE('',#3009,#681);
#588=LINE('',#3011,#682);
#589=LINE('',#3013,#683);
#590=LINE('',#3014,#684);
#591=LINE('',#3017,#685);
#592=LINE('',#3019,#686);
#593=LINE('',#3020,#687);
#594=LINE('',#3023,#688);
#595=LINE('',#3025,#689);
#596=LINE('',#3026,#690);
#597=LINE('',#3029,#691);
#598=LINE('',#3031,#692);
#599=LINE('',#3032,#693);
#600=LINE('',#3035,#694);
#601=LINE('',#3037,#695);
#602=LINE('',#3038,#696);
#603=LINE('',#3040,#697);
#604=LINE('',#3041,#698);
#605=LINE('',#3053,#699);
#606=LINE('',#3057,#700);
#607=LINE('',#3061,#701);
#608=LINE('',#3068,#702);
#609=LINE('',#3070,#703);
#681=VECTOR('',#2412,1.);
#682=VECTOR('',#2413,1.);
#683=VECTOR('',#2414,1.);
#684=VECTOR('',#2415,1.);
#685=VECTOR('',#2418,1.);
#686=VECTOR('',#2419,1.);
#687=VECTOR('',#2420,1.);
#688=VECTOR('',#2423,1.);
#689=VECTOR('',#2424,1.);
#690=VECTOR('',#2425,1.);
#691=VECTOR('',#2428,1.);
#692=VECTOR('',#2429,1.);
#693=VECTOR('',#2430,1.);
#694=VECTOR('',#2433,1.);
#695=VECTOR('',#2434,1.);
#696=VECTOR('',#2435,1.);
#697=VECTOR('',#2438,1.);
#698=VECTOR('',#2439,1.);
#699=VECTOR('',#2456,0.325);
#700=VECTOR('',#2461,0.35);
#701=VECTOR('',#2466,0.335);
#702=VECTOR('',#2475,0.21);
#703=VECTOR('',#2478,0.2);
#752=CIRCLE('',#2039,0.1954);
#753=CIRCLE('',#2041,0.3);
#754=CIRCLE('',#2043,0.35);
#755=CIRCLE('',#2045,0.35);
#756=CIRCLE('',#2047,0.32);
#757=CIRCLE('',#2049,0.22);
#758=CIRCLE('',#2051,0.1954);
#890=VERTEX_POINT('',#3007);
#891=VERTEX_POINT('',#3008);
#892=VERTEX_POINT('',#3010);
#893=VERTEX_POINT('',#3012);
#894=VERTEX_POINT('',#3016);
#895=VERTEX_POINT('',#3018);
#896=VERTEX_POINT('',#3022);
#897=VERTEX_POINT('',#3024);
#898=VERTEX_POINT('',#3028);
#899=VERTEX_POINT('',#3030);
#900=VERTEX_POINT('',#3034);
#901=VERTEX_POINT('',#3036);
#902=VERTEX_POINT('',#3045);
#903=VERTEX_POINT('',#3048);
#904=VERTEX_POINT('',#3051);
#905=VERTEX_POINT('',#3055);
#906=VERTEX_POINT('',#3059);
#907=VERTEX_POINT('',#3063);
#908=VERTEX_POINT('',#3066);
#1070=EDGE_CURVE('',#890,#891,#587,.T.);
#1071=EDGE_CURVE('',#891,#892,#588,.T.);
#1072=EDGE_CURVE('',#892,#893,#589,.T.);
#1073=EDGE_CURVE('',#890,#893,#590,.T.);
#1074=EDGE_CURVE('',#891,#894,#591,.T.);
#1075=EDGE_CURVE('',#894,#895,#592,.T.);
#1076=EDGE_CURVE('',#895,#892,#593,.T.);
#1077=EDGE_CURVE('',#894,#896,#594,.T.);
#1078=EDGE_CURVE('',#896,#897,#595,.T.);
#1079=EDGE_CURVE('',#897,#895,#596,.T.);
#1080=EDGE_CURVE('',#896,#898,#597,.T.);
#1081=EDGE_CURVE('',#898,#899,#598,.T.);
#1082=EDGE_CURVE('',#899,#897,#599,.T.);
#1083=EDGE_CURVE('',#898,#900,#600,.T.);
#1084=EDGE_CURVE('',#900,#901,#601,.T.);
#1085=EDGE_CURVE('',#901,#899,#602,.T.);
#1086=EDGE_CURVE('',#900,#890,#603,.T.);
#1087=EDGE_CURVE('',#893,#901,#604,.T.);
#1088=EDGE_CURVE('',#902,#902,#752,.T.);
#1089=EDGE_CURVE('',#903,#903,#753,.T.);
#1090=EDGE_CURVE('',#904,#904,#754,.T.);
#1091=EDGE_CURVE('',#904,#903,#605,.T.);
#1092=EDGE_CURVE('',#905,#905,#755,.T.);
#1093=EDGE_CURVE('',#905,#904,#606,.T.);
#1094=EDGE_CURVE('',#906,#906,#756,.T.);
#1095=EDGE_CURVE('',#906,#905,#607,.T.);
#1096=EDGE_CURVE('',#907,#907,#757,.T.);
#1097=EDGE_CURVE('',#908,#908,#758,.F.);
#1098=EDGE_CURVE('',#908,#907,#608,.T.);
#1099=EDGE_CURVE('',#902,#908,#609,.T.);
#1367=ORIENTED_EDGE('',*,*,#1070,.T.);
#1368=ORIENTED_EDGE('',*,*,#1071,.T.);
#1369=ORIENTED_EDGE('',*,*,#1072,.T.);
#1370=ORIENTED_EDGE('',*,*,#1073,.F.);
#1371=ORIENTED_EDGE('',*,*,#1074,.T.);
#1372=ORIENTED_EDGE('',*,*,#1075,.T.);
#1373=ORIENTED_EDGE('',*,*,#1076,.T.);
#1374=ORIENTED_EDGE('',*,*,#1071,.F.);
#1375=ORIENTED_EDGE('',*,*,#1077,.T.);
#1376=ORIENTED_EDGE('',*,*,#1078,.T.);
#1377=ORIENTED_EDGE('',*,*,#1079,.T.);
#1378=ORIENTED_EDGE('',*,*,#1075,.F.);
#1379=ORIENTED_EDGE('',*,*,#1080,.T.);
#1380=ORIENTED_EDGE('',*,*,#1081,.T.);
#1381=ORIENTED_EDGE('',*,*,#1082,.T.);
#1382=ORIENTED_EDGE('',*,*,#1078,.F.);
#1383=ORIENTED_EDGE('',*,*,#1083,.T.);
#1384=ORIENTED_EDGE('',*,*,#1084,.T.);
#1385=ORIENTED_EDGE('',*,*,#1085,.T.);
#1386=ORIENTED_EDGE('',*,*,#1081,.F.);
#1387=ORIENTED_EDGE('',*,*,#1086,.T.);
#1388=ORIENTED_EDGE('',*,*,#1073,.T.);
#1389=ORIENTED_EDGE('',*,*,#1087,.T.);
#1390=ORIENTED_EDGE('',*,*,#1084,.F.);
#1391=ORIENTED_EDGE('',*,*,#1086,.F.);
#1392=ORIENTED_EDGE('',*,*,#1083,.F.);
#1393=ORIENTED_EDGE('',*,*,#1080,.F.);
#1394=ORIENTED_EDGE('',*,*,#1077,.F.);
#1395=ORIENTED_EDGE('',*,*,#1074,.F.);
#1396=ORIENTED_EDGE('',*,*,#1070,.F.);
#1397=ORIENTED_EDGE('',*,*,#1087,.F.);
#1398=ORIENTED_EDGE('',*,*,#1072,.F.);
#1399=ORIENTED_EDGE('',*,*,#1076,.F.);
#1400=ORIENTED_EDGE('',*,*,#1079,.F.);
#1401=ORIENTED_EDGE('',*,*,#1082,.F.);
#1402=ORIENTED_EDGE('',*,*,#1085,.F.);
#1403=ORIENTED_EDGE('',*,*,#1088,.F.);
#1404=ORIENTED_EDGE('',*,*,#1089,.F.);
#1405=ORIENTED_EDGE('',*,*,#1090,.F.);
#1406=ORIENTED_EDGE('',*,*,#1091,.T.);
#1407=ORIENTED_EDGE('',*,*,#1089,.T.);
#1408=ORIENTED_EDGE('',*,*,#1091,.F.);
#1409=ORIENTED_EDGE('',*,*,#1092,.F.);
#1410=ORIENTED_EDGE('',*,*,#1093,.T.);
#1411=ORIENTED_EDGE('',*,*,#1090,.T.);
#1412=ORIENTED_EDGE('',*,*,#1093,.F.);
#1413=ORIENTED_EDGE('',*,*,#1094,.F.);
#1414=ORIENTED_EDGE('',*,*,#1095,.T.);
#1415=ORIENTED_EDGE('',*,*,#1092,.T.);
#1416=ORIENTED_EDGE('',*,*,#1095,.F.);
#1417=ORIENTED_EDGE('',*,*,#1094,.T.);
#1418=ORIENTED_EDGE('',*,*,#1096,.F.);
#1419=ORIENTED_EDGE('',*,*,#1097,.F.);
#1420=ORIENTED_EDGE('',*,*,#1098,.T.);
#1421=ORIENTED_EDGE('',*,*,#1096,.T.);
#1422=ORIENTED_EDGE('',*,*,#1098,.F.);
#1423=ORIENTED_EDGE('',*,*,#1088,.T.);
#1424=ORIENTED_EDGE('',*,*,#1099,.T.);
#1425=ORIENTED_EDGE('',*,*,#1097,.T.);
#1426=ORIENTED_EDGE('',*,*,#1099,.F.);
#1674=CYLINDRICAL_SURFACE('',#2044,0.35);
#1675=CYLINDRICAL_SURFACE('',#2052,0.1954);
#1731=ADVANCED_FACE('',(#313),#243,.F.);
#1732=ADVANCED_FACE('',(#314),#244,.F.);
#1733=ADVANCED_FACE('',(#315),#245,.F.);
#1734=ADVANCED_FACE('',(#316),#246,.F.);
#1735=ADVANCED_FACE('',(#317),#247,.F.);
#1736=ADVANCED_FACE('',(#318),#248,.F.);
#1737=ADVANCED_FACE('',(#319),#249,.F.);
#1738=ADVANCED_FACE('',(#320),#250,.F.);
#1739=ADVANCED_FACE('',(#321),#251,.F.);
#1740=ADVANCED_FACE('',(#322),#252,.T.);
#1741=ADVANCED_FACE('',(#323),#113,.T.);
#1742=ADVANCED_FACE('',(#324),#1674,.T.);
#1743=ADVANCED_FACE('',(#325),#114,.T.);
#1744=ADVANCED_FACE('',(#326,#203),#253,.T.);
#1745=ADVANCED_FACE('',(#327),#115,.T.);
#1746=ADVANCED_FACE('',(#328),#1675,.T.);
#1811=CLOSED_SHELL('',(#1731,#1732,#1733,#1734,#1735,#1736,#1737,#1738));
#1812=CLOSED_SHELL('',(#1739,#1740,#1741,#1742,#1743,#1744,#1745,#1746));
#2029=AXIS2_PLACEMENT_3D('',#3005,#2408,#2409);
#2030=AXIS2_PLACEMENT_3D('',#3006,#2410,#2411);
#2031=AXIS2_PLACEMENT_3D('',#3015,#2416,#2417);
#2032=AXIS2_PLACEMENT_3D('',#3021,#2421,#2422);
#2033=AXIS2_PLACEMENT_3D('',#3027,#2426,#2427);
#2034=AXIS2_PLACEMENT_3D('',#3033,#2431,#2432);
#2035=AXIS2_PLACEMENT_3D('',#3039,#2436,#2437);
#2036=AXIS2_PLACEMENT_3D('',#3042,#2440,#2441);
#2037=AXIS2_PLACEMENT_3D('',#3043,#2442,#2443);
#2038=AXIS2_PLACEMENT_3D('',#3044,#2444,#2445);
#2039=AXIS2_PLACEMENT_3D('',#3046,#2446,#2447);
#2040=AXIS2_PLACEMENT_3D('',#3047,#2448,#2449);
#2041=AXIS2_PLACEMENT_3D('',#3049,#2450,#2451);
#2042=AXIS2_PLACEMENT_3D('',#3050,#2452,#2453);
#2043=AXIS2_PLACEMENT_3D('',#3052,#2454,#2455);
#2044=AXIS2_PLACEMENT_3D('',#3054,#2457,#2458);
#2045=AXIS2_PLACEMENT_3D('',#3056,#2459,#2460);
#2046=AXIS2_PLACEMENT_3D('',#3058,#2462,#2463);
#2047=AXIS2_PLACEMENT_3D('',#3060,#2464,#2465);
#2048=AXIS2_PLACEMENT_3D('',#3062,#2467,#2468);
#2049=AXIS2_PLACEMENT_3D('',#3064,#2469,#2470);
#2050=AXIS2_PLACEMENT_3D('',#3065,#2471,#2472);
#2051=AXIS2_PLACEMENT_3D('',#3067,#2473,#2474);
#2052=AXIS2_PLACEMENT_3D('',#3069,#2476,#2477);
#2408=DIRECTION('axis',(0.,0.,1.));
#2409=DIRECTION('refdir',(1.,0.,0.));
#2410=DIRECTION('center_axis',(0.866025403784439,0.,-0.5));
#2411=DIRECTION('ref_axis',(0.5,0.,0.866025403784439));
#2412=DIRECTION('',(-0.5,0.,-0.866025403784439));
#2413=DIRECTION('',(0.,-1.,0.));
#2414=DIRECTION('',(0.5,0.,0.866025403784439));
#2415=DIRECTION('',(0.,-1.,0.));
#2416=DIRECTION('center_axis',(1.60246890531964E-16,0.,-1.));
#2417=DIRECTION('ref_axis',(1.,0.,1.60246890531964E-16));
#2418=DIRECTION('',(-1.,0.,-1.60246890531964E-16));
#2419=DIRECTION('',(0.,-1.,0.));
#2420=DIRECTION('',(1.,0.,1.60246890531964E-16));
#2421=DIRECTION('center_axis',(-0.866025403784439,0.,-0.5));
#2422=DIRECTION('ref_axis',(0.5,0.,-0.866025403784439));
#2423=DIRECTION('',(-0.5,0.,0.866025403784439));
#2424=DIRECTION('',(0.,-1.,0.));
#2425=DIRECTION('',(0.5,0.,-0.866025403784439));
#2426=DIRECTION('center_axis',(-0.866025403784439,0.,0.5));
#2427=DIRECTION('ref_axis',(-0.5,0.,-0.866025403784439));
#2428=DIRECTION('',(0.5,0.,0.866025403784439));
#2429=DIRECTION('',(0.,-1.,0.));
#2430=DIRECTION('',(-0.5,0.,-0.866025403784439));
#2431=DIRECTION('center_axis',(-1.60246890531964E-16,0.,1.));
#2432=DIRECTION('ref_axis',(-1.,0.,-1.60246890531964E-16));
#2433=DIRECTION('',(1.,0.,1.60246890531964E-16));
#2434=DIRECTION('',(0.,-1.,0.));
#2435=DIRECTION('',(-1.,0.,-1.60246890531964E-16));
#2436=DIRECTION('center_axis',(0.866025403784439,0.,0.5));
#2437=DIRECTION('ref_axis',(-0.5,0.,0.866025403784439));
#2438=DIRECTION('',(0.5,0.,-0.866025403784439));
#2439=DIRECTION('',(-0.5,0.,0.866025403784439));
#2440=DIRECTION('center_axis',(0.,1.,0.));
#2441=DIRECTION('ref_axis',(1.,0.,0.));
#2442=DIRECTION('center_axis',(0.,-1.,0.));
#2443=DIRECTION('ref_axis',(0.,0.,-1.));
#2444=DIRECTION('center_axis',(0.,1.,0.));
#2445=DIRECTION('ref_axis',(1.,0.,0.));
#2446=DIRECTION('center_axis',(0.,1.,0.));
#2447=DIRECTION('ref_axis',(1.,0.,0.));
#2448=DIRECTION('center_axis',(0.,1.,0.));
#2449=DIRECTION('ref_axis',(0.,0.,1.));
#2450=DIRECTION('center_axis',(0.,-1.,0.));
#2451=DIRECTION('ref_axis',(1.,0.,0.));
#2452=DIRECTION('center_axis',(0.,-1.,0.));
#2453=DIRECTION('ref_axis',(1.,0.,0.));
#2454=DIRECTION('center_axis',(0.,-1.,0.));
#2455=DIRECTION('ref_axis',(1.,0.,0.));
#2456=DIRECTION('',(0.707106781186547,0.707106781186548,8.65956056235493E-17));
#2457=DIRECTION('center_axis',(0.,-1.,0.));
#2458=DIRECTION('ref_axis',(1.,0.,0.));
#2459=DIRECTION('center_axis',(0.,-1.,0.));
#2460=DIRECTION('ref_axis',(1.,0.,0.));
#2461=DIRECTION('',(0.,1.,0.));
#2462=DIRECTION('center_axis',(0.,1.,0.));
#2463=DIRECTION('ref_axis',(1.,0.,0.));
#2464=DIRECTION('center_axis',(0.,-1.,0.));
#2465=DIRECTION('ref_axis',(1.,0.,0.));
#2466=DIRECTION('',(-0.707106781186547,0.707106781186548,-8.65956056235493E-17));
#2467=DIRECTION('center_axis',(0.,-1.,0.));
#2468=DIRECTION('ref_axis',(0.,0.,-1.));
#2469=DIRECTION('center_axis',(0.,-1.,0.));
#2470=DIRECTION('ref_axis',(1.,0.,0.));
#2471=DIRECTION('center_axis',(0.,1.,0.));
#2472=DIRECTION('ref_axis',(1.,0.,0.));
#2473=DIRECTION('center_axis',(0.,1.,0.));
#2474=DIRECTION('ref_axis',(1.,0.,0.));
#2475=DIRECTION('',(-0.447213595499958,0.894427190999916,-5.47678698264203E-17));
#2476=DIRECTION('center_axis',(0.,-1.,0.));
#2477=DIRECTION('ref_axis',(1.,0.,0.));
#2478=DIRECTION('',(0.,1.,0.));
#3005=CARTESIAN_POINT('',(0.,0.,0.));
#3006=CARTESIAN_POINT('Origin',(0.0866025403784439,-0.4,-0.15));
#3007=CARTESIAN_POINT('',(0.173205080756888,-0.4,0.));
#3008=CARTESIAN_POINT('',(0.0866025403784439,-0.4,-0.15));
#3009=CARTESIAN_POINT('',(0.173205080756888,-0.4,0.));
#3010=CARTESIAN_POINT('',(0.0866025403784439,-0.64,-0.15));
#3011=CARTESIAN_POINT('',(0.0866025403784439,-0.4,-0.15));
#3012=CARTESIAN_POINT('',(0.173205080756888,-0.64,0.));
#3013=CARTESIAN_POINT('',(0.173205080756888,-0.64,0.));
#3014=CARTESIAN_POINT('',(0.173205080756888,-0.4,0.));
#3015=CARTESIAN_POINT('Origin',(-0.0866025403784438,-0.4,-0.15));
#3016=CARTESIAN_POINT('',(-0.0866025403784438,-0.4,-0.15));
#3017=CARTESIAN_POINT('',(0.0866025403784439,-0.4,-0.15));
#3018=CARTESIAN_POINT('',(-0.0866025403784438,-0.64,-0.15));
#3019=CARTESIAN_POINT('',(-0.0866025403784438,-0.4,-0.15));
#3020=CARTESIAN_POINT('',(0.0866025403784439,-0.64,-0.15));
#3021=CARTESIAN_POINT('Origin',(-0.173205080756888,-0.4,-2.77555756156289E-17));
#3022=CARTESIAN_POINT('',(-0.173205080756888,-0.4,-2.12115047744981E-17));
#3023=CARTESIAN_POINT('',(-0.0866025403784438,-0.4,-0.15));
#3024=CARTESIAN_POINT('',(-0.173205080756888,-0.64,-2.77555756156289E-17));
#3025=CARTESIAN_POINT('',(-0.173205080756888,-0.4,-2.12115047744981E-17));
#3026=CARTESIAN_POINT('',(-0.0866025403784438,-0.64,-0.15));
#3027=CARTESIAN_POINT('Origin',(-0.0866025403784439,-0.4,0.15));
#3028=CARTESIAN_POINT('',(-0.0866025403784439,-0.4,0.15));
#3029=CARTESIAN_POINT('',(-0.173205080756888,-0.4,-2.12115047744981E-17));
#3030=CARTESIAN_POINT('',(-0.0866025403784439,-0.64,0.15));
#3031=CARTESIAN_POINT('',(-0.0866025403784439,-0.4,0.15));
#3032=CARTESIAN_POINT('',(-0.173205080756888,-0.64,-2.12115047744981E-17));
#3033=CARTESIAN_POINT('Origin',(0.0866025403784439,-0.4,0.15));
#3034=CARTESIAN_POINT('',(0.0866025403784439,-0.4,0.15));
#3035=CARTESIAN_POINT('',(-0.0866025403784439,-0.4,0.15));
#3036=CARTESIAN_POINT('',(0.0866025403784439,-0.64,0.15));
#3037=CARTESIAN_POINT('',(0.0866025403784439,-0.4,0.15));
#3038=CARTESIAN_POINT('',(-0.0866025403784439,-0.64,0.15));
#3039=CARTESIAN_POINT('Origin',(0.173205080756888,-0.4,0.));
#3040=CARTESIAN_POINT('',(0.0866025403784439,-0.4,0.15));
#3041=CARTESIAN_POINT('',(0.0866025403784439,-0.64,0.15));
#3042=CARTESIAN_POINT('Origin',(0.,-0.4,-2.77555756156289E-17));
#3043=CARTESIAN_POINT('Origin',(0.,-0.64,-2.77555756156289E-17));
#3044=CARTESIAN_POINT('Origin',(0.,-1.,0.));
#3045=CARTESIAN_POINT('',(-0.1954,-1.,2.39295984553393E-17));
#3046=CARTESIAN_POINT('Origin',(0.,-1.,0.));
#3047=CARTESIAN_POINT('Origin',(0.3,0.4,0.));
#3048=CARTESIAN_POINT('',(-0.3,0.4,-3.67394039744206E-17));
#3049=CARTESIAN_POINT('Origin',(0.,0.4,0.));
#3050=CARTESIAN_POINT('Origin',(0.,0.375,0.));
#3051=CARTESIAN_POINT('',(-0.35,0.35,-4.28626379701573E-17));
#3052=CARTESIAN_POINT('Origin',(0.,0.35,0.));
#3053=CARTESIAN_POINT('',(-0.325,0.375,-3.9801020972289E-17));
#3054=CARTESIAN_POINT('Origin',(0.,0.19,0.));
#3055=CARTESIAN_POINT('',(-0.35,0.03,-4.28626379701574E-17));
#3056=CARTESIAN_POINT('Origin',(0.,0.03,0.));
#3057=CARTESIAN_POINT('',(-0.35,0.19,-4.28626379701574E-17));
#3058=CARTESIAN_POINT('Origin',(0.,0.0149999999999999,0.));
#3059=CARTESIAN_POINT('',(-0.32,-3.29597460435593E-17,-3.91886975727153E-17));
#3060=CARTESIAN_POINT('Origin',(0.,0.,0.));
#3061=CARTESIAN_POINT('',(-0.335,0.0149999999999999,-4.10256677714363E-17));
#3062=CARTESIAN_POINT('Origin',(0.22,0.,0.));
#3063=CARTESIAN_POINT('',(-0.22,-6.93889390390723E-18,-2.69422295812418E-17));
#3064=CARTESIAN_POINT('Origin',(0.,0.,0.));
#3065=CARTESIAN_POINT('Origin',(0.,-0.02,0.));
#3066=CARTESIAN_POINT('',(-0.1954,-0.0492,2.39295984553393E-17));
#3067=CARTESIAN_POINT('Origin',(0.,-0.0492,0.));
#3068=CARTESIAN_POINT('',(-0.21,-0.02,-2.57175827820944E-17));
#3069=CARTESIAN_POINT('Origin',(0.,-0.8,0.));
#3070=CARTESIAN_POINT('',(-0.1954,-0.8,-2.39295984553393E-17));
#3661=UNCERTAINTY_MEASURE_WITH_UNIT(LENGTH_MEASURE(0.001),#3689,
'DISTANCE_ACCURACY_VALUE',
'Maximum model space distance between geometric entities at asserted c
onnectivities');
#3671=UNCERTAINTY_MEASURE_WITH_UNIT(LENGTH_MEASURE(0.001),#3689,
'DISTANCE_ACCURACY_VALUE',
'Maximum model space distance between geometric entities at asserted c
onnectivities');
#3678=(
GEOMETRIC_REPRESENTATION_CONTEXT(3)
GLOBAL_UNCERTAINTY_ASSIGNED_CONTEXT((#3661))
GLOBAL_UNIT_ASSIGNED_CONTEXT((#3689,#3691,#3692))
REPRESENTATION_CONTEXT('','3D')
);
#3688=(
GEOMETRIC_REPRESENTATION_CONTEXT(3)
GLOBAL_UNCERTAINTY_ASSIGNED_CONTEXT((#3671))
GLOBAL_UNIT_ASSIGNED_CONTEXT((#3689,#3691,#3692))
REPRESENTATION_CONTEXT('','3D')
);
#3689=(
LENGTH_UNIT()
NAMED_UNIT(*)
SI_UNIT(.CENTI.,.METRE.)
);
#3691=(
NAMED_UNIT(*)
PLANE_ANGLE_UNIT()
SI_UNIT($,.RADIAN.)
);
#3692=(
NAMED_UNIT(*)
SI_UNIT($,.STERADIAN.)
SOLID_ANGLE_UNIT()
);
#3699=SHAPE_DEFINITION_REPRESENTATION(#3715,#3749);
#3715=PRODUCT_DEFINITION_SHAPE('',$,#3766);
#3749=SHAPE_REPRESENTATION('',(#2029),#3678);
#3759=PRODUCT_DEFINITION_CONTEXT('part definition',#3809,'design');
#3766=PRODUCT_DEFINITION('M4x10 Cap Screw','M4x10 Cap Screw',#3782,#3759);
#3782=PRODUCT_DEFINITION_FORMATION('',$,#3817);
#3809=APPLICATION_CONTEXT(
'Core Data for Automotive Mechanical Design Process');
#3810=PRODUCT_CONTEXT('part definition',#3809,'mechanical');
#3817=PRODUCT('M4x10 Cap Screw','M4x10 Cap Screw','M4x10 Cap Screw',(#3810));
#3897=COLOUR_RGB('Black',0.12,0.14,0.17);
#3898=FILL_AREA_STYLE_COLOUR('',#3897);
#3899=FILL_AREA_STYLE('',(#3898));
#3900=SURFACE_STYLE_FILL_AREA(#3899);
#3901=SURFACE_SIDE_STYLE('',(#3900));
#3902=SURFACE_STYLE_USAGE(.BOTH.,#3901);
#3903=PRESENTATION_STYLE_ASSIGNMENT((#3902));
ENDSEC;
END-ISO-10303-21;
